ISO-10303-21;
HEADER;
/* Generated by software containing ST-Developer
 * from STEP Tools, Inc. (www.steptools.com) 
 */

FILE_DESCRIPTION(
/* description */ ('Telescoping shaft support with lock collar'),
/* implementation_level */ '2;1');

FILE_NAME(
/* name */ 'Cap Screw - M5x20.step',
/* time_stamp */ '2026-10-27T10:48:51-07:00',
/* author */ (''),
/* organization */ (''),
/* preprocessor_version */ 'ST-DEVELOPER v20.2',
/* originating_system */ 'Autodesk Translation Framework v15.17.0.0',
/* authorisation */ '');

FILE_SCHEMA (('AUTOMOTIVE_DESIGN { 1 0 10303 214 3 1 1 }'));
ENDSEC;

DATA;
#10=MECHANICAL_DESIGN_GEOMETRIC_PRESENTATION_REPRESENTATION('',(#252),#7349);
#167=ORIENTED_CLOSED_SHELL('',*,#3976,.F.);
#169=CONICAL_SURFACE('',#4496,0.4,0.785398163397448);
#170=CONICAL_SURFACE('',#4500,0.41,0.785398163397448);
#171=CONICAL_SURFACE('',#4504,0.26,0.463647609000806);
#172=CONICAL_SURFACE('',#4508,0.225,0.785398163397448);
#181=BREP_WITH_VOIDS('Body1',#3975,(#167));
#212=SHAPE_REPRESENTATION_RELATIONSHIP('SRR','None',#7454,#232);
#232=ADVANCED_BREP_SHAPE_REPRESENTATION('',(#181),#7338);
#252=STYLED_ITEM('',(#7634),#181);
#337=FACE_BOUND('',#912,.T.);
#433=PLANE('',#4494);
#434=PLANE('',#4502);
#435=PLANE('',#4510);
#436=PLANE('',#4511);
#437=PLANE('',#4512);
#438=PLANE('',#4513);
#439=PLANE('',#4514);
#440=PLANE('',#4515);
#441=PLANE('',#4516);
#442=PLANE('',#4517);
#443=PLANE('',#4518);
#623=FACE_OUTER_BOUND('',#907,.T.);
#624=FACE_OUTER_BOUND('',#908,.T.);
#625=FACE_OUTER_BOUND('',#909,.T.);
#626=FACE_OUTER_BOUND('',#910,.T.);
#627=FACE_OUTER_BOUND('',#911,.T.);
#628=FACE_OUTER_BOUND('',#913,.T.);
#629=FACE_OUTER_BOUND('',#914,.T.);
#630=FACE_OUTER_BOUND('',#915,.T.);
#631=FACE_OUTER_BOUND('',#916,.T.);
#632=FACE_OUTER_BOUND('',#917,.T.);
#633=FACE_OUTER_BOUND('',#918,.T.);
#634=FACE_OUTER_BOUND('',#919,.T.);
#635=FACE_OUTER_BOUND('',#920,.T.);
#636=FACE_OUTER_BOUND('',#921,.T.);
#637=FACE_OUTER_BOUND('',#922,.T.);
#638=FACE_OUTER_BOUND('',#923,.T.);
#639=FACE_OUTER_BOUND('',#924,.T.);
#907=EDGE_LOOP('',(#3268));
#908=EDGE_LOOP('',(#3269,#3270,#3271,#3272));
#909=EDGE_LOOP('',(#3273,#3274,#3275,#3276));
#910=EDGE_LOOP('',(#3277,#3278,#3279,#3280));
#911=EDGE_LOOP('',(#3281));
#912=EDGE_LOOP('',(#3282));
#913=EDGE_LOOP('',(#3283,#3284,#3285,#3286));
#914=EDGE_LOOP('',(#3287,#3288,#3289,#3290));
#915=EDGE_LOOP('',(#3291,#3292,#3293,#3294));
#916=EDGE_LOOP('',(#3295));
#917=EDGE_LOOP('',(#3296,#3297,#3298,#3299));
#918=EDGE_LOOP('',(#3300,#3301,#3302,#3303));
#919=EDGE_LOOP('',(#3304,#3305,#3306,#3307));
#920=EDGE_LOOP('',(#3308,#3309,#3310,#3311));
#921=EDGE_LOOP('',(#3312,#3313,#3314,#3315));
#922=EDGE_LOOP('',(#3316,#3317,#3318,#3319));
#923=EDGE_LOOP('',(#3320,#3321,#3322,#3323,#3324,#3325));
#924=EDGE_LOOP('',(#3326,#3327,#3328,#3329,#3330,#3331));
#1191=LINE('',#6727,#1471);
#1192=LINE('',#6731,#1472);
#1193=LINE('',#6735,#1473);
#1194=LINE('',#6742,#1474);
#1195=LINE('',#6746,#1475);
#1196=LINE('',#6750,#1476);
#1197=LINE('',#6755,#1477);
#1198=LINE('',#6757,#1478);
#1199=LINE('',#6759,#1479);
#1200=LINE('',#6760,#1480);
#1201=LINE('',#6763,#1481);
#1202=LINE('',#6765,#1482);
#1203=LINE('',#6766,#1483);
#1204=LINE('',#6769,#1484);
#1205=LINE('',#6771,#1485);
#1206=LINE('',#6772,#1486);
#1207=LINE('',#6775,#1487);
#1208=LINE('',#6777,#1488);
#1209=LINE('',#6778,#1489);
#1210=LINE('',#6781,#1490);
#1211=LINE('',#6783,#1491);
#1212=LINE('',#6784,#1492);
#1213=LINE('',#6786,#1493);
#1214=LINE('',#6787,#1494);
#1471=VECTOR('',#5453,0.4);
#1472=VECTOR('',#5458,0.425);
#1473=VECTOR('',#5463,0.41);
#1474=VECTOR('',#5472,0.26);
#1475=VECTOR('',#5477,0.25);
#1476=VECTOR('',#5482,0.225);
#1477=VECTOR('',#5487,1.);
#1478=VECTOR('',#5488,1.);
#1479=VECTOR('',#5489,1.);
#1480=VECTOR('',#5490,1.);
#1481=VECTOR('',#5493,1.);
#1482=VECTOR('',#5494,1.);
#1483=VECTOR('',#5495,1.);
#1484=VECTOR('',#5498,1.);
#1485=VECTOR('',#5499,1.);
#1486=VECTOR('',#5500,1.);
#1487=VECTOR('',#5503,1.);
#1488=VECTOR('',#5504,1.);
#1489=VECTOR('',#5505,1.);
#1490=VECTOR('',#5508,1.);
#1491=VECTOR('',#5509,1.);
#1492=VECTOR('',#5510,1.);
#1493=VECTOR('',#5513,1.);
#1494=VECTOR('',#5514,1.);
#1732=CIRCLE('',#4495,0.375);
#1733=CIRCLE('',#4497,0.425);
#1734=CIRCLE('',#4499,0.425);
#1735=CIRCLE('',#4501,0.395);
#1736=CIRCLE('',#4503,0.27);
#1737=CIRCLE('',#4505,0.24505);
#1738=CIRCLE('',#4507,0.24505);
#1739=CIRCLE('',#4509,0.2);
#2007=VERTEX_POINT('',#6722);
#2008=VERTEX_POINT('',#6725);
#2009=VERTEX_POINT('',#6729);
#2010=VERTEX_POINT('',#6733);
#2011=VERTEX_POINT('',#6737);
#2012=VERTEX_POINT('',#6740);
#2013=VERTEX_POINT('',#6744);
#2014=VERTEX_POINT('',#6748);
#2015=VERTEX_POINT('',#6753);
#2016=VERTEX_POINT('',#6754);
#2017=VERTEX_POINT('',#6756);
#2018=VERTEX_POINT('',#6758);
#2019=VERTEX_POINT('',#6762);
#2020=VERTEX_POINT('',#6764);
#2021=VERTEX_POINT('',#6768);
#2022=VERTEX_POINT('',#6770);
#2023=VERTEX_POINT('',#6774);
#2024=VERTEX_POINT('',#6776);
#2025=VERTEX_POINT('',#6780);
#2026=VERTEX_POINT('',#6782);
#2446=EDGE_CURVE('',#2007,#2007,#1732,.T.);
#2447=EDGE_CURVE('',#2008,#2008,#1733,.T.);
#2448=EDGE_CURVE('',#2008,#2007,#1191,.T.);
#2449=EDGE_CURVE('',#2009,#2009,#1734,.T.);
#2450=EDGE_CURVE('',#2009,#2008,#1192,.T.);
#2451=EDGE_CURVE('',#2010,#2010,#1735,.T.);
#2452=EDGE_CURVE('',#2010,#2009,#1193,.T.);
#2453=EDGE_CURVE('',#2011,#2011,#1736,.T.);
#2454=EDGE_CURVE('',#2012,#2012,#1737,.F.);
#2455=EDGE_CURVE('',#2012,#2011,#1194,.T.);
#2456=EDGE_CURVE('',#2013,#2013,#1738,.F.);
#2457=EDGE_CURVE('',#2013,#2012,#1195,.T.);
#2458=EDGE_CURVE('',#2014,#2014,#1739,.T.);
#2459=EDGE_CURVE('',#2014,#2013,#1196,.T.);
#2460=EDGE_CURVE('',#2015,#2016,#1197,.T.);
#2461=EDGE_CURVE('',#2016,#2017,#1198,.T.);
#2462=EDGE_CURVE('',#2017,#2018,#1199,.T.);
#2463=EDGE_CURVE('',#2015,#2018,#1200,.T.);
#2464=EDGE_CURVE('',#2016,#2019,#1201,.T.);
#2465=EDGE_CURVE('',#2019,#2020,#1202,.T.);
#2466=EDGE_CURVE('',#2020,#2017,#1203,.T.);
#2467=EDGE_CURVE('',#2019,#2021,#1204,.T.);
#2468=EDGE_CURVE('',#2021,#2022,#1205,.T.);
#2469=EDGE_CURVE('',#2022,#2020,#1206,.T.);
#2470=EDGE_CURVE('',#2021,#2023,#1207,.T.);
#2471=EDGE_CURVE('',#2023,#2024,#1208,.T.);
#2472=EDGE_CURVE('',#2024,#2022,#1209,.T.);
#2473=EDGE_CURVE('',#2023,#2025,#1210,.T.);
#2474=EDGE_CURVE('',#2025,#2026,#1211,.T.);
#2475=EDGE_CURVE('',#2026,#2024,#1212,.T.);
#2476=EDGE_CURVE('',#2025,#2015,#1213,.T.);
#2477=EDGE_CURVE('',#2018,#2026,#1214,.T.);
#3268=ORIENTED_EDGE('',*,*,#2446,.F.);
#3269=ORIENTED_EDGE('',*,*,#2447,.F.);
#3270=ORIENTED_EDGE('',*,*,#2448,.T.);
#3271=ORIENTED_EDGE('',*,*,#2446,.T.);
#3272=ORIENTED_EDGE('',*,*,#2448,.F.);
#3273=ORIENTED_EDGE('',*,*,#2449,.F.);
#3274=ORIENTED_EDGE('',*,*,#2450,.T.);
#3275=ORIENTED_EDGE('',*,*,#2447,.T.);
#3276=ORIENTED_EDGE('',*,*,#2450,.F.);
#3277=ORIENTED_EDGE('',*,*,#2451,.F.);
#3278=ORIENTED_EDGE('',*,*,#2452,.T.);
#3279=ORIENTED_EDGE('',*,*,#2449,.T.);
#3280=ORIENTED_EDGE('',*,*,#2452,.F.);
#3281=ORIENTED_EDGE('',*,*,#2451,.T.);
#3282=ORIENTED_EDGE('',*,*,#2453,.F.);
#3283=ORIENTED_EDGE('',*,*,#2454,.F.);
#3284=ORIENTED_EDGE('',*,*,#2455,.T.);
#3285=ORIENTED_EDGE('',*,*,#2453,.T.);
#3286=ORIENTED_EDGE('',*,*,#2455,.F.);
#3287=ORIENTED_EDGE('',*,*,#2456,.F.);
#3288=ORIENTED_EDGE('',*,*,#2457,.T.);
#3289=ORIENTED_EDGE('',*,*,#2454,.T.);
#3290=ORIENTED_EDGE('',*,*,#2457,.F.);
#3291=ORIENTED_EDGE('',*,*,#2458,.F.);
#3292=ORIENTED_EDGE('',*,*,#2459,.T.);
#3293=ORIENTED_EDGE('',*,*,#2456,.T.);
#3294=ORIENTED_EDGE('',*,*,#2459,.F.);
#3295=ORIENTED_EDGE('',*,*,#2458,.T.);
#3296=ORIENTED_EDGE('',*,*,#2460,.T.);
#3297=ORIENTED_EDGE('',*,*,#2461,.T.);
#3298=ORIENTED_EDGE('',*,*,#2462,.T.);
#3299=ORIENTED_EDGE('',*,*,#2463,.F.);
#3300=ORIENTED_EDGE('',*,*,#2464,.T.);
#3301=ORIENTED_EDGE('',*,*,#2465,.T.);
#3302=ORIENTED_EDGE('',*,*,#2466,.T.);
#3303=ORIENTED_EDGE('',*,*,#2461,.F.);
#3304=ORIENTED_EDGE('',*,*,#2467,.T.);
#3305=ORIENTED_EDGE('',*,*,#2468,.T.);
#3306=ORIENTED_EDGE('',*,*,#2469,.T.);
#3307=ORIENTED_EDGE('',*,*,#2465,.F.);
#3308=ORIENTED_EDGE('',*,*,#2470,.T.);
#3309=ORIENTED_EDGE('',*,*,#2471,.T.);
#3310=ORIENTED_EDGE('',*,*,#2472,.T.);
#3311=ORIENTED_EDGE('',*,*,#2468,.F.);
#3312=ORIENTED_EDGE('',*,*,#2473,.T.);
#3313=ORIENTED_EDGE('',*,*,#2474,.T.);
#3314=ORIENTED_EDGE('',*,*,#2475,.T.);
#3315=ORIENTED_EDGE('',*,*,#2471,.F.);
#3316=ORIENTED_EDGE('',*,*,#2476,.T.);
#3317=ORIENTED_EDGE('',*,*,#2463,.T.);
#3318=ORIENTED_EDGE('',*,*,#2477,.T.);
#3319=ORIENTED_EDGE('',*,*,#2474,.F.);
#3320=ORIENTED_EDGE('',*,*,#2476,.F.);
#3321=ORIENTED_EDGE('',*,*,#2473,.F.);
#3322=ORIENTED_EDGE('',*,*,#2470,.F.);
#3323=ORIENTED_EDGE('',*,*,#2467,.F.);
#3324=ORIENTED_EDGE('',*,*,#2464,.F.);
#3325=ORIENTED_EDGE('',*,*,#2460,.F.);
#3326=ORIENTED_EDGE('',*,*,#2477,.F.);
#3327=ORIENTED_EDGE('',*,*,#2462,.F.);
#3328=ORIENTED_EDGE('',*,*,#2466,.F.);
#3329=ORIENTED_EDGE('',*,*,#2469,.F.);
#3330=ORIENTED_EDGE('',*,*,#2472,.F.);
#3331=ORIENTED_EDGE('',*,*,#2475,.F.);
#3714=CYLINDRICAL_SURFACE('',#4498,0.425);
#3715=CYLINDRICAL_SURFACE('',#4506,0.24505);
#3866=ADVANCED_FACE('',(#623),#433,.T.);
#3867=ADVANCED_FACE('',(#624),#169,.T.);
#3868=ADVANCED_FACE('',(#625),#3714,.T.);
#3869=ADVANCED_FACE('',(#626),#170,.T.);
#3870=ADVANCED_FACE('',(#627,#337),#434,.T.);
#3871=ADVANCED_FACE('',(#628),#171,.T.);
#3872=ADVANCED_FACE('',(#629),#3715,.T.);
#3873=ADVANCED_FACE('',(#630),#172,.T.);
#3874=ADVANCED_FACE('',(#631),#435,.T.);
#3875=ADVANCED_FACE('',(#632),#436,.F.);
#3876=ADVANCED_FACE('',(#633),#437,.F.);
#3877=ADVANCED_FACE('',(#634),#438,.F.);
#3878=ADVANCED_FACE('',(#635),#439,.F.);
#3879=ADVANCED_FACE('',(#636),#440,.F.);
#3880=ADVANCED_FACE('',(#637),#441,.F.);
#3881=ADVANCED_FACE('',(#638),#442,.F.);
#3882=ADVANCED_FACE('',(#639),#443,.F.);
#3975=CLOSED_SHELL('',(#3866,#3867,#3868,#3869,#3870,#3871,#3872,#3873,
#3874));
#3976=CLOSED_SHELL('',(#3875,#3876,#3877,#3878,#3879,#3880,#3881,#3882));
#4493=AXIS2_PLACEMENT_3D('',#6720,#5443,#5444);
#4494=AXIS2_PLACEMENT_3D('',#6721,#5445,#5446);
#4495=AXIS2_PLACEMENT_3D('',#6723,#5447,#5448);
#4496=AXIS2_PLACEMENT_3D('',#6724,#5449,#5450);
#4497=AXIS2_PLACEMENT_3D('',#6726,#5451,#5452);
#4498=AXIS2_PLACEMENT_3D('',#6728,#5454,#5455);
#4499=AXIS2_PLACEMENT_3D('',#6730,#5456,#5457);
#4500=AXIS2_PLACEMENT_3D('',#6732,#5459,#5460);
#4501=AXIS2_PLACEMENT_3D('',#6734,#5461,#5462);
#4502=AXIS2_PLACEMENT_3D('',#6736,#5464,#5465);
#4503=AXIS2_PLACEMENT_3D('',#6738,#5466,#5467);
#4504=AXIS2_PLACEMENT_3D('',#6739,#5468,#5469);
#4505=AXIS2_PLACEMENT_3D('',#6741,#5470,#5471);
#4506=AXIS2_PLACEMENT_3D('',#6743,#5473,#5474);
#4507=AXIS2_PLACEMENT_3D('',#6745,#5475,#5476);
#4508=AXIS2_PLACEMENT_3D('',#6747,#5478,#5479);
#4509=AXIS2_PLACEMENT_3D('',#6749,#5480,#5481);
#4510=AXIS2_PLACEMENT_3D('',#6751,#5483,#5484);
#4511=AXIS2_PLACEMENT_3D('',#6752,#5485,#5486);
#4512=AXIS2_PLACEMENT_3D('',#6761,#5491,#5492);
#4513=AXIS2_PLACEMENT_3D('',#6767,#5496,#5497);
#4514=AXIS2_PLACEMENT_3D('',#6773,#5501,#5502);
#4515=AXIS2_PLACEMENT_3D('',#6779,#5506,#5507);
#4516=AXIS2_PLACEMENT_3D('',#6785,#5511,#5512);
#4517=AXIS2_PLACEMENT_3D('',#6788,#5515,#5516);
#4518=AXIS2_PLACEMENT_3D('',#6789,#5517,#5518);
#5443=DIRECTION('axis',(0.,0.,1.));
#5444=DIRECTION('refdir',(1.,0.,0.));
#5445=DIRECTION('center_axis',(0.,1.,0.));
#5446=DIRECTION('ref_axis',(0.,0.,1.));
#5447=DIRECTION('center_axis',(0.,-1.,0.));
#5448=DIRECTION('ref_axis',(1.,0.,0.));
#5449=DIRECTION('center_axis',(0.,-1.,0.));
#5450=DIRECTION('ref_axis',(1.,0.,0.));
#5451=DIRECTION('center_axis',(0.,-1.,0.));
#5452=DIRECTION('ref_axis',(1.,0.,0.));
#5453=DIRECTION('',(0.707106781186548,0.707106781186547,8.65956056235493E-17));
#5454=DIRECTION('center_axis',(0.,-1.,0.));
#5455=DIRECTION('ref_axis',(1.,0.,0.));
#5456=DIRECTION('center_axis',(0.,-1.,0.));
#5457=DIRECTION('ref_axis',(1.,0.,0.));
#5458=DIRECTION('',(0.,1.,0.));
#5459=DIRECTION('center_axis',(0.,1.,0.));
#5460=DIRECTION('ref_axis',(1.,0.,0.));
#5461=DIRECTION('center_axis',(0.,-1.,0.));
#5462=DIRECTION('ref_axis',(1.,0.,0.));
#5463=DIRECTION('',(-0.707106781186547,0.707106781186548,-8.65956056235493E-17));
#5464=DIRECTION('center_axis',(0.,-1.,0.));
#5465=DIRECTION('ref_axis',(0.,0.,-1.));
#5466=DIRECTION('center_axis',(0.,-1.,0.));
#5467=DIRECTION('ref_axis',(1.,0.,0.));
#5468=DIRECTION('center_axis',(0.,1.,0.));
#5469=DIRECTION('ref_axis',(1.,0.,0.));
#5470=DIRECTION('center_axis',(0.,1.,0.));
#5471=DIRECTION('ref_axis',(1.,0.,0.));
#5472=DIRECTION('',(-0.447213595499958,0.894427190999916,-5.47678698264203E-17));
#5473=DIRECTION('center_axis',(0.,-1.,0.));
#5474=DIRECTION('ref_axis',(1.,0.,0.));
#5475=DIRECTION('center_axis',(0.,1.,0.));
#5476=DIRECTION('ref_axis',(1.,0.,0.));
#5477=DIRECTION('',(0.,1.,0.));
#5478=DIRECTION('center_axis',(0.,1.,0.));
#5479=DIRECTION('ref_axis',(1.,0.,0.));
#5480=DIRECTION('center_axis',(0.,-1.,0.));
#5481=DIRECTION('ref_axis',(1.,0.,0.));
#5482=DIRECTION('',(-0.707106781186547,0.707106781186548,-8.65956056235493E-17));
#5483=DIRECTION('center_axis',(0.,-1.,0.));
#5484=DIRECTION('ref_axis',(0.,0.,-1.));
#5485=DIRECTION('center_axis',(0.866025403784439,0.,-0.5));
#5486=DIRECTION('ref_axis',(0.5,0.,0.866025403784439));
#5487=DIRECTION('',(-0.5,0.,-0.866025403784439));
#5488=DIRECTION('',(0.,-1.,0.));
#5489=DIRECTION('',(0.5,0.,0.866025403784439));
#5490=DIRECTION('',(0.,-1.,0.));
#5491=DIRECTION('center_axis',(1.20185167898973E-16,0.,-1.));
#5492=DIRECTION('ref_axis',(1.,0.,1.20185167898973E-16));
#5493=DIRECTION('',(-1.,0.,-1.20185167898973E-16));
#5494=DIRECTION('',(0.,-1.,0.));
#5495=DIRECTION('',(1.,0.,1.20185167898973E-16));
#5496=DIRECTION('center_axis',(-0.866025403784439,0.,-0.5));
#5497=DIRECTION('ref_axis',(0.5,0.,-0.866025403784439));
#5498=DIRECTION('',(-0.5,0.,0.866025403784439));
#5499=DIRECTION('',(0.,-1.,0.));
#5500=DIRECTION('',(0.5,0.,-0.866025403784439));
#5501=DIRECTION('center_axis',(-0.866025403784439,0.,0.5));
#5502=DIRECTION('ref_axis',(-0.5,0.,-0.866025403784439));
#5503=DIRECTION('',(0.5,0.,0.866025403784439));
#5504=DIRECTION('',(0.,-1.,0.));
#5505=DIRECTION('',(-0.5,0.,-0.866025403784439));
#5506=DIRECTION('center_axis',(-2.40370335797945E-16,0.,1.));
#5507=DIRECTION('ref_axis',(-1.,0.,-2.40370335797945E-16));
#5508=DIRECTION('',(1.,0.,2.40370335797945E-16));
#5509=DIRECTION('',(0.,-1.,0.));
#5510=DIRECTION('',(-1.,0.,-2.40370335797945E-16));
#5511=DIRECTION('center_axis',(0.866025403784439,0.,0.5));
#5512=DIRECTION('ref_axis',(-0.5,0.,0.866025403784439));
#5513=DIRECTION('',(0.5,0.,-0.866025403784439));
#5514=DIRECTION('',(-0.5,0.,0.866025403784439));
#5515=DIRECTION('center_axis',(0.,1.,0.));
#5516=DIRECTION('ref_axis',(1.,0.,0.));
#5517=DIRECTION('center_axis',(0.,-1.,0.));
#5518=DIRECTION('ref_axis',(0.,0.,-1.));
#6720=CARTESIAN_POINT('',(0.,0.,0.));
#6721=CARTESIAN_POINT('Origin',(0.375,0.5,0.));
#6722=CARTESIAN_POINT('',(-0.375,0.5,-4.59242549680257E-17));
#6723=CARTESIAN_POINT('Origin',(0.,0.5,0.));
#6724=CARTESIAN_POINT('Origin',(0.,0.475,0.));
#6725=CARTESIAN_POINT('',(-0.425,0.45,-5.20474889637625E-17));
#6726=CARTESIAN_POINT('Origin',(0.,0.45,0.));
#6727=CARTESIAN_POINT('',(-0.4,0.475,-4.89858719658941E-17));
#6728=CARTESIAN_POINT('Origin',(0.,0.24,0.));
#6729=CARTESIAN_POINT('',(-0.425,0.0299999999999998,-5.20474889637625E-17));
#6730=CARTESIAN_POINT('Origin',(0.,0.0299999999999998,0.));
#6731=CARTESIAN_POINT('',(-0.425,0.24,-5.20474889637625E-17));
#6732=CARTESIAN_POINT('Origin',(0.,0.0150000000000001,0.));
#6733=CARTESIAN_POINT('',(-0.395,4.85722573273506E-17,-4.83735485663204E-17));
#6734=CARTESIAN_POINT('Origin',(0.,0.,0.));
#6735=CARTESIAN_POINT('',(-0.41,0.0150000000000001,-5.02105187650415E-17));
#6736=CARTESIAN_POINT('Origin',(0.27,0.,0.));
#6737=CARTESIAN_POINT('',(-0.27,0.,-3.30654635769785E-17));
#6738=CARTESIAN_POINT('Origin',(0.,0.,0.));
#6739=CARTESIAN_POINT('Origin',(0.,-0.02,0.));
#6740=CARTESIAN_POINT('',(-0.24505,-0.0498999999999999,3.00099698131059E-17));
#6741=CARTESIAN_POINT('Origin',(0.,-0.0498999999999999,0.));
#6742=CARTESIAN_POINT('',(-0.26,-0.02,-3.18408167778312E-17));
#6743=CARTESIAN_POINT('Origin',(0.,-0.995,0.));
#6744=CARTESIAN_POINT('',(-0.24505,-1.95495,3.00099698131059E-17));
#6745=CARTESIAN_POINT('Origin',(0.,-1.95495,0.));
#6746=CARTESIAN_POINT('',(-0.24505,-0.995,-3.00099698131059E-17));
#6747=CARTESIAN_POINT('Origin',(0.,-1.975,0.));
#6748=CARTESIAN_POINT('',(-0.2,-2.,-2.44929359829471E-17));
#6749=CARTESIAN_POINT('Origin',(0.,-2.,0.));
#6750=CARTESIAN_POINT('',(-0.225,-1.975,-2.75545529808154E-17));
#6751=CARTESIAN_POINT('Origin',(0.,-2.,0.));
#6752=CARTESIAN_POINT('Origin',(0.115470053837925,-0.5,-0.2));
#6753=CARTESIAN_POINT('',(0.23094010767585,-0.5,0.));
#6754=CARTESIAN_POINT('',(0.115470053837925,-0.5,-0.2));
#6755=CARTESIAN_POINT('',(0.23094010767585,-0.5,0.));
#6756=CARTESIAN_POINT('',(0.115470053837925,-0.8,-0.2));
#6757=CARTESIAN_POINT('',(0.115470053837925,-0.5,-0.2));
#6758=CARTESIAN_POINT('',(0.23094010767585,-0.8,0.));
#6759=CARTESIAN_POINT('',(0.23094010767585,-0.8,0.));
#6760=CARTESIAN_POINT('',(0.23094010767585,-0.5,0.));
#6761=CARTESIAN_POINT('Origin',(-0.115470053837925,-0.5,-0.2));
#6762=CARTESIAN_POINT('',(-0.115470053837925,-0.5,-0.2));
#6763=CARTESIAN_POINT('',(0.115470053837925,-0.5,-0.2));
#6764=CARTESIAN_POINT('',(-0.115470053837925,-0.8,-0.2));
#6765=CARTESIAN_POINT('',(-0.115470053837925,-0.5,-0.2));
#6766=CARTESIAN_POINT('',(0.115470053837925,-0.8,-0.2));
#6767=CARTESIAN_POINT('Origin',(-0.23094010767585,-0.5,-2.77555756156289E-17));
#6768=CARTESIAN_POINT('',(-0.23094010767585,-0.5,-2.82820063659975E-17));
#6769=CARTESIAN_POINT('',(-0.115470053837925,-0.5,-0.2));
#6770=CARTESIAN_POINT('',(-0.23094010767585,-0.8,-2.77555756156289E-17));
#6771=CARTESIAN_POINT('',(-0.23094010767585,-0.5,-2.82820063659975E-17));
#6772=CARTESIAN_POINT('',(-0.115470053837925,-0.8,-0.2));
#6773=CARTESIAN_POINT('Origin',(-0.115470053837925,-0.5,0.2));
#6774=CARTESIAN_POINT('',(-0.115470053837925,-0.5,0.2));
#6775=CARTESIAN_POINT('',(-0.23094010767585,-0.5,-2.82820063659975E-17));
#6776=CARTESIAN_POINT('',(-0.115470053837925,-0.8,0.2));
#6777=CARTESIAN_POINT('',(-0.115470053837925,-0.5,0.2));
#6778=CARTESIAN_POINT('',(-0.23094010767585,-0.8,-2.82820063659975E-17));
#6779=CARTESIAN_POINT('Origin',(0.115470053837925,-0.5,0.2));
#6780=CARTESIAN_POINT('',(0.115470053837925,-0.5,0.2));
#6781=CARTESIAN_POINT('',(-0.115470053837925,-0.5,0.2));
#6782=CARTESIAN_POINT('',(0.115470053837925,-0.8,0.2));
#6783=CARTESIAN_POINT('',(0.115470053837925,-0.5,0.2));
#6784=CARTESIAN_POINT('',(-0.115470053837925,-0.8,0.2));
#6785=CARTESIAN_POINT('Origin',(0.23094010767585,-0.5,0.));
#6786=CARTESIAN_POINT('',(0.115470053837925,-0.5,0.2));
#6787=CARTESIAN_POINT('',(0.115470053837925,-0.8,0.2));
#6788=CARTESIAN_POINT('Origin',(0.,-0.5,0.));
#6789=CARTESIAN_POINT('Origin',(0.,-0.8,0.));
#7313=UNCERTAINTY_MEASURE_WITH_UNIT(LENGTH_MEASURE(0.001),#7350,
'DISTANCE_ACCURACY_VALUE',
'Maximum model space distance between geometric entities at asserted c
onnectivities');
#7324=UNCERTAINTY_MEASURE_WITH_UNIT(LENGTH_MEASURE(0.001),#7350,
'DISTANCE_ACCURACY_VALUE',
'Maximum model space distance between geometric entities at asserted c
onnectivities');
#7338=(
GEOMETRIC_REPRESENTATION_CONTEXT(3)
GLOBAL_UNCERTAINTY_ASSIGNED_CONTEXT((#7313))
GLOBAL_UNIT_ASSIGNED_CONTEXT((#7350,#7352,#7353))
REPRESENTATION_CONTEXT('','3D')
);
#7349=(
GEOMETRIC_REPRESENTATION_CONTEXT(3)
GLOBAL_UNCERTAINTY_ASSIGNED_CONTEXT((#7324))
GLOBAL_UNIT_ASSIGNED_CONTEXT((#7350,#7352,#7353))
REPRESENTATION_CONTEXT('','3D')
);
#7350=(
LENGTH_UNIT()
NAMED_UNIT(*)
SI_UNIT(.CENTI.,.METRE.)
);
#7352=(
NAMED_UNIT(*)
PLANE_ANGLE_UNIT()
SI_UNIT($,.RADIAN.)
);
#7353=(
NAMED_UNIT(*)
SI_UNIT($,.STERADIAN.)
SOLID_ANGLE_UNIT()
);
#7367=SHAPE_DEFINITION_REPRESENTATION(#7391,#7454);
#7391=PRODUCT_DEFINITION_SHAPE('',$,#7479);
#7454=SHAPE_REPRESENTATION('',(#4493),#7338);
#7465=PRODUCT_DEFINITION_CONTEXT('part definition',#7539,'design');
#7479=PRODUCT_DEFINITION('Cap Screw - M5x20','Cap Screw - M5x20',#7503,
#7465);
#7503=PRODUCT_DEFINITION_FORMATION('',$,#7554);
#7539=APPLICATION_CONTEXT(
'Core Data for Automotive Mechanical Design Process');
#7540=PRODUCT_CONTEXT('part definition',#7539,'mechanical');
#7554=PRODUCT('Cap Screw - M5x20','Cap Screw - M5x20',
'Cap Screw - M5x20',(#7540));
#7628=COLOUR_RGB('Black',0.12,0.14,0.17);
#7629=FILL_AREA_STYLE_COLOUR('',#7628);
#7630=FILL_AREA_STYLE('',(#7629));
#7631=SURFACE_STYLE_FILL_AREA(#7630);
#7632=SURFACE_SIDE_STYLE('',(#7631));
#7633=SURFACE_STYLE_USAGE(.BOTH.,#7632);
#7634=PRESENTATION_STYLE_ASSIGNMENT((#7633));
ENDSEC;
END-ISO-10303-21;
